ISO-10303-21;
HEADER;
/* Generated by software containing ST-Developer
 * from STEP Tools, Inc. (www.steptools.com) 
 */

FILE_DESCRIPTION(
/* description */ ('Ball-type isolation valve (generic)'),
/* implementation_level */ '2;1');

FILE_NAME(
/* name */ 'Hex Nut - M5.step',
/* time_stamp */ '2026-10-27T10:53:05-07:00',
/* author */ (''),
/* organization */ (''),
/* preprocessor_version */ 'ST-DEVELOPER v20.2',
/* originating_system */ 'Autodesk Translation Framework v15.17.0.0',
/* authorisation */ '');

FILE_SCHEMA (('AUTOMOTIVE_DESIGN { 1 0 10303 214 3 1 1 }'));
ENDSEC;

DATA;
#10=MECHANICAL_DESIGN_GEOMETRIC_PRESENTATION_REPRESENTATION('',(#294),#7425);
#191=(
BOUNDED_CURVE()
B_SPLINE_CURVE(2,(#6817,#6818,#6819),.UNSPECIFIED.,.F.,.F.)
B_SPLINE_CURVE_WITH_KNOTS((3,3),(0.140651836354967,0.670383167684795),
 .UNSPECIFIED.)
CURVE()
GEOMETRIC_REPRESENTATION_ITEM()
RATIONAL_B_SPLINE_CURVE((1.11602540378444,1.28867513459481,1.11602540378444))
REPRESENTATION_ITEM('')
);
#192=(
BOUNDED_CURVE()
B_SPLINE_CURVE(2,(#6821,#6822,#6823),.UNSPECIFIED.,.F.,.F.)
B_SPLINE_CURVE_WITH_KNOTS((3,3),(0.140651836354967,0.670383167684795),
 .UNSPECIFIED.)
CURVE()
GEOMETRIC_REPRESENTATION_ITEM()
RATIONAL_B_SPLINE_CURVE((1.11602540378444,1.28867513459481,1.11602540378444))
REPRESENTATION_ITEM('')
);
#193=(
BOUNDED_CURVE()
B_SPLINE_CURVE(2,(#6828,#6829,#6830),.UNSPECIFIED.,.F.,.F.)
B_SPLINE_CURVE_WITH_KNOTS((3,3),(0.140651836354967,0.670383167684795),
 .UNSPECIFIED.)
CURVE()
GEOMETRIC_REPRESENTATION_ITEM()
RATIONAL_B_SPLINE_CURVE((1.11602540378444,1.28867513459481,1.11602540378444))
REPRESENTATION_ITEM('')
);
#194=(
BOUNDED_CURVE()
B_SPLINE_CURVE(2,(#6832,#6833,#6834),.UNSPECIFIED.,.F.,.F.)
B_SPLINE_CURVE_WITH_KNOTS((3,3),(0.140651836354967,0.670383167684795),
 .UNSPECIFIED.)
CURVE()
GEOMETRIC_REPRESENTATION_ITEM()
RATIONAL_B_SPLINE_CURVE((1.11602540378444,1.28867513459481,1.11602540378444))
REPRESENTATION_ITEM('')
);
#195=(
BOUNDED_CURVE()
B_SPLINE_CURVE(2,(#6836,#6837,#6838),.UNSPECIFIED.,.F.,.F.)
B_SPLINE_CURVE_WITH_KNOTS((3,3),(0.140651836354967,0.670383167684795),
 .UNSPECIFIED.)
CURVE()
GEOMETRIC_REPRESENTATION_ITEM()
RATIONAL_B_SPLINE_CURVE((1.11602540378444,1.28867513459481,1.11602540378444))
REPRESENTATION_ITEM('')
);
#196=(
BOUNDED_CURVE()
B_SPLINE_CURVE(2,(#6839,#6840,#6841),.UNSPECIFIED.,.F.,.F.)
B_SPLINE_CURVE_WITH_KNOTS((3,3),(0.140651836354967,0.670383167684795),
 .UNSPECIFIED.)
CURVE()
GEOMETRIC_REPRESENTATION_ITEM()
RATIONAL_B_SPLINE_CURVE((1.11602540378444,1.28867513459481,1.11602540378444))
REPRESENTATION_ITEM('')
);
#197=(
BOUNDED_CURVE()
B_SPLINE_CURVE(2,(#6848,#6849,#6850),.UNSPECIFIED.,.F.,.F.)
B_SPLINE_CURVE_WITH_KNOTS((3,3),(0.140651836354967,0.670383167684795),
 .UNSPECIFIED.)
CURVE()
GEOMETRIC_REPRESENTATION_ITEM()
RATIONAL_B_SPLINE_CURVE((1.11602540378444,1.28867513459481,1.11602540378444))
REPRESENTATION_ITEM('')
);
#198=(
BOUNDED_CURVE()
B_SPLINE_CURVE(2,(#6852,#6853,#6854),.UNSPECIFIED.,.F.,.F.)
B_SPLINE_CURVE_WITH_KNOTS((3,3),(0.140651836354967,0.670383167684796),
 .UNSPECIFIED.)
CURVE()
GEOMETRIC_REPRESENTATION_ITEM()
RATIONAL_B_SPLINE_CURVE((1.11602540378444,1.28867513459481,1.11602540378444))
REPRESENTATION_ITEM('')
);
#199=(
BOUNDED_CURVE()
B_SPLINE_CURVE(2,(#6856,#6857,#6858),.UNSPECIFIED.,.F.,.F.)
B_SPLINE_CURVE_WITH_KNOTS((3,3),(0.140651836354967,0.670383167684795),
 .UNSPECIFIED.)
CURVE()
GEOMETRIC_REPRESENTATION_ITEM()
RATIONAL_B_SPLINE_CURVE((1.11602540378444,1.28867513459481,1.11602540378444))
REPRESENTATION_ITEM('')
);
#200=(
BOUNDED_CURVE()
B_SPLINE_CURVE(2,(#6860,#6861,#6862),.UNSPECIFIED.,.F.,.F.)
B_SPLINE_CURVE_WITH_KNOTS((3,3),(0.140651836354967,0.670383167684795),
 .UNSPECIFIED.)
CURVE()
GEOMETRIC_REPRESENTATION_ITEM()
RATIONAL_B_SPLINE_CURVE((1.11602540378444,1.28867513459482,1.11602540378444))
REPRESENTATION_ITEM('')
);
#201=(
BOUNDED_CURVE()
B_SPLINE_CURVE(2,(#6864,#6865,#6866),.UNSPECIFIED.,.F.,.F.)
B_SPLINE_CURVE_WITH_KNOTS((3,3),(0.140651836354967,0.670383167684795),
 .UNSPECIFIED.)
CURVE()
GEOMETRIC_REPRESENTATION_ITEM()
RATIONAL_B_SPLINE_CURVE((1.11602540378444,1.28867513459481,1.11602540378444))
REPRESENTATION_ITEM('')
);
#202=(
BOUNDED_CURVE()
B_SPLINE_CURVE(2,(#6867,#6868,#6869),.UNSPECIFIED.,.F.,.F.)
B_SPLINE_CURVE_WITH_KNOTS((3,3),(0.140651836354967,0.670383167684795),
 .UNSPECIFIED.)
CURVE()
GEOMETRIC_REPRESENTATION_ITEM()
RATIONAL_B_SPLINE_CURVE((1.11602540378444,1.28867513459481,1.11602540378444))
REPRESENTATION_ITEM('')
);
#207=CONICAL_SURFACE('',#4683,0.47094010767585,1.0471975511966);
#208=CONICAL_SURFACE('',#4685,0.47094010767585,1.0471975511966);
#242=SHAPE_REPRESENTATION_RELATIONSHIP('SRR','None',#7552,#268);
#268=ADVANCED_BREP_SHAPE_REPRESENTATION('',(#319),#7415);
#294=STYLED_ITEM('',(#7751),#319);
#319=MANIFOLD_SOLID_BREP('Body1',#4100);
#403=FACE_BOUND('',#1051,.T.);
#404=FACE_BOUND('',#1053,.T.);
#496=PLANE('',#4687);
#497=PLANE('',#4688);
#498=PLANE('',#4689);
#499=PLANE('',#4693);
#500=PLANE('',#4694);
#501=PLANE('',#4695);
#502=PLANE('',#4696);
#503=PLANE('',#4697);
#720=FACE_OUTER_BOUND('',#1041,.T.);
#721=FACE_OUTER_BOUND('',#1042,.T.);
#722=FACE_OUTER_BOUND('',#1043,.T.);
#723=FACE_OUTER_BOUND('',#1044,.T.);
#724=FACE_OUTER_BOUND('',#1045,.T.);
#725=FACE_OUTER_BOUND('',#1046,.T.);
#726=FACE_OUTER_BOUND('',#1047,.T.);
#727=FACE_OUTER_BOUND('',#1048,.T.);
#728=FACE_OUTER_BOUND('',#1049,.T.);
#729=FACE_OUTER_BOUND('',#1050,.T.);
#730=FACE_OUTER_BOUND('',#1052,.T.);
#1041=EDGE_LOOP('',(#3319,#3320,#3321,#3322,#3323,#3324,#3325,#3326,#3327));
#1042=EDGE_LOOP('',(#3328,#3329,#3330,#3331,#3332,#3333,#3334,#3335,#3336));
#1043=EDGE_LOOP('',(#3337,#3338,#3339,#3340));
#1044=EDGE_LOOP('',(#3341,#3342,#3343,#3344));
#1045=EDGE_LOOP('',(#3345,#3346,#3347,#3348));
#1046=EDGE_LOOP('',(#3349,#3350,#3351,#3352));
#1047=EDGE_LOOP('',(#3353,#3354,#3355,#3356));
#1048=EDGE_LOOP('',(#3357,#3358,#3359,#3360));
#1049=EDGE_LOOP('',(#3361,#3362,#3363,#3364));
#1050=EDGE_LOOP('',(#3365));
#1051=EDGE_LOOP('',(#3366));
#1052=EDGE_LOOP('',(#3367));
#1053=EDGE_LOOP('',(#3368));
#1313=LINE('',#6825,#1621);
#1314=LINE('',#6846,#1622);
#1315=LINE('',#6871,#1623);
#1316=LINE('',#6872,#1624);
#1317=LINE('',#6874,#1625);
#1318=LINE('',#6876,#1626);
#1319=LINE('',#6881,#1627);
#1320=LINE('',#6884,#1628);
#1321=LINE('',#6886,#1629);
#1621=VECTOR('',#5616,0.47094010767585);
#1622=VECTOR('',#5623,0.47094010767585);
#1623=VECTOR('',#5626,1.);
#1624=VECTOR('',#5627,1.);
#1625=VECTOR('',#5630,1.);
#1626=VECTOR('',#5633,1.);
#1627=VECTOR('',#5638,0.25);
#1628=VECTOR('',#5643,1.);
#1629=VECTOR('',#5646,1.);
#1905=CIRCLE('',#4684,0.38);
#1906=CIRCLE('',#4686,0.38);
#1907=CIRCLE('',#4691,0.2117);
#1908=CIRCLE('',#4692,0.2117);
#2137=VERTEX_POINT('',#6815);
#2138=VERTEX_POINT('',#6816);
#2139=VERTEX_POINT('',#6820);
#2140=VERTEX_POINT('',#6824);
#2141=VERTEX_POINT('',#6827);
#2142=VERTEX_POINT('',#6831);
#2143=VERTEX_POINT('',#6835);
#2144=VERTEX_POINT('',#6843);
#2145=VERTEX_POINT('',#6845);
#2146=VERTEX_POINT('',#6847);
#2147=VERTEX_POINT('',#6851);
#2148=VERTEX_POINT('',#6855);
#2149=VERTEX_POINT('',#6859);
#2150=VERTEX_POINT('',#6863);
#2151=VERTEX_POINT('',#6878);
#2152=VERTEX_POINT('',#6880);
#2552=EDGE_CURVE('',#2137,#2138,#191,.T.);
#2553=EDGE_CURVE('',#2139,#2137,#192,.T.);
#2554=EDGE_CURVE('',#2139,#2140,#1313,.T.);
#2555=EDGE_CURVE('',#2140,#2140,#1905,.T.);
#2556=EDGE_CURVE('',#2141,#2139,#193,.T.);
#2557=EDGE_CURVE('',#2142,#2141,#194,.T.);
#2558=EDGE_CURVE('',#2143,#2142,#195,.T.);
#2559=EDGE_CURVE('',#2138,#2143,#196,.T.);
#2560=EDGE_CURVE('',#2144,#2144,#1906,.T.);
#2561=EDGE_CURVE('',#2144,#2145,#1314,.T.);
#2562=EDGE_CURVE('',#2146,#2145,#197,.T.);
#2563=EDGE_CURVE('',#2147,#2146,#198,.T.);
#2564=EDGE_CURVE('',#2148,#2147,#199,.T.);
#2565=EDGE_CURVE('',#2149,#2148,#200,.T.);
#2566=EDGE_CURVE('',#2150,#2149,#201,.T.);
#2567=EDGE_CURVE('',#2145,#2150,#202,.T.);
#2568=EDGE_CURVE('',#2141,#2150,#1315,.T.);
#2569=EDGE_CURVE('',#2142,#2149,#1316,.T.);
#2570=EDGE_CURVE('',#2139,#2145,#1317,.T.);
#2571=EDGE_CURVE('',#2137,#2146,#1318,.T.);
#2572=EDGE_CURVE('',#2151,#2151,#1907,.F.);
#2573=EDGE_CURVE('',#2151,#2152,#1319,.T.);
#2574=EDGE_CURVE('',#2152,#2152,#1908,.F.);
#2575=EDGE_CURVE('',#2138,#2147,#1320,.T.);
#2576=EDGE_CURVE('',#2143,#2148,#1321,.T.);
#3319=ORIENTED_EDGE('',*,*,#2552,.F.);
#3320=ORIENTED_EDGE('',*,*,#2553,.F.);
#3321=ORIENTED_EDGE('',*,*,#2554,.T.);
#3322=ORIENTED_EDGE('',*,*,#2555,.F.);
#3323=ORIENTED_EDGE('',*,*,#2554,.F.);
#3324=ORIENTED_EDGE('',*,*,#2556,.F.);
#3325=ORIENTED_EDGE('',*,*,#2557,.F.);
#3326=ORIENTED_EDGE('',*,*,#2558,.F.);
#3327=ORIENTED_EDGE('',*,*,#2559,.F.);
#3328=ORIENTED_EDGE('',*,*,#2560,.F.);
#3329=ORIENTED_EDGE('',*,*,#2561,.T.);
#3330=ORIENTED_EDGE('',*,*,#2562,.F.);
#3331=ORIENTED_EDGE('',*,*,#2563,.F.);
#3332=ORIENTED_EDGE('',*,*,#2564,.F.);
#3333=ORIENTED_EDGE('',*,*,#2565,.F.);
#3334=ORIENTED_EDGE('',*,*,#2566,.F.);
#3335=ORIENTED_EDGE('',*,*,#2567,.F.);
#3336=ORIENTED_EDGE('',*,*,#2561,.F.);
#3337=ORIENTED_EDGE('',*,*,#2557,.T.);
#3338=ORIENTED_EDGE('',*,*,#2568,.T.);
#3339=ORIENTED_EDGE('',*,*,#2566,.T.);
#3340=ORIENTED_EDGE('',*,*,#2569,.F.);
#3341=ORIENTED_EDGE('',*,*,#2556,.T.);
#3342=ORIENTED_EDGE('',*,*,#2570,.T.);
#3343=ORIENTED_EDGE('',*,*,#2567,.T.);
#3344=ORIENTED_EDGE('',*,*,#2568,.F.);
#3345=ORIENTED_EDGE('',*,*,#2553,.T.);
#3346=ORIENTED_EDGE('',*,*,#2571,.T.);
#3347=ORIENTED_EDGE('',*,*,#2562,.T.);
#3348=ORIENTED_EDGE('',*,*,#2570,.F.);
#3349=ORIENTED_EDGE('',*,*,#2572,.F.);
#3350=ORIENTED_EDGE('',*,*,#2573,.T.);
#3351=ORIENTED_EDGE('',*,*,#2574,.T.);
#3352=ORIENTED_EDGE('',*,*,#2573,.F.);
#3353=ORIENTED_EDGE('',*,*,#2552,.T.);
#3354=ORIENTED_EDGE('',*,*,#2575,.T.);
#3355=ORIENTED_EDGE('',*,*,#2563,.T.);
#3356=ORIENTED_EDGE('',*,*,#2571,.F.);
#3357=ORIENTED_EDGE('',*,*,#2558,.T.);
#3358=ORIENTED_EDGE('',*,*,#2569,.T.);
#3359=ORIENTED_EDGE('',*,*,#2565,.T.);
#3360=ORIENTED_EDGE('',*,*,#2576,.F.);
#3361=ORIENTED_EDGE('',*,*,#2559,.T.);
#3362=ORIENTED_EDGE('',*,*,#2576,.T.);
#3363=ORIENTED_EDGE('',*,*,#2564,.T.);
#3364=ORIENTED_EDGE('',*,*,#2575,.F.);
#3365=ORIENTED_EDGE('',*,*,#2560,.T.);
#3366=ORIENTED_EDGE('',*,*,#2572,.T.);
#3367=ORIENTED_EDGE('',*,*,#2555,.T.);
#3368=ORIENTED_EDGE('',*,*,#2574,.F.);
#3820=CYLINDRICAL_SURFACE('',#4690,0.2117);
#3974=ADVANCED_FACE('',(#720),#207,.T.);
#3975=ADVANCED_FACE('',(#721),#208,.T.);
#3976=ADVANCED_FACE('',(#722),#496,.T.);
#3977=ADVANCED_FACE('',(#723),#497,.T.);
#3978=ADVANCED_FACE('',(#724),#498,.T.);
#3979=ADVANCED_FACE('',(#725),#3820,.F.);
#3980=ADVANCED_FACE('',(#726),#499,.T.);
#3981=ADVANCED_FACE('',(#727),#500,.T.);
#3982=ADVANCED_FACE('',(#728),#501,.T.);
#3983=ADVANCED_FACE('',(#729,#403),#502,.T.);
#3984=ADVANCED_FACE('',(#730,#404),#503,.F.);
#4100=CLOSED_SHELL('',(#3974,#3975,#3976,#3977,#3978,#3979,#3980,#3981,
#3982,#3983,#3984));
#4682=AXIS2_PLACEMENT_3D('',#6813,#5612,#5613);
#4683=AXIS2_PLACEMENT_3D('',#6814,#5614,#5615);
#4684=AXIS2_PLACEMENT_3D('',#6826,#5617,#5618);
#4685=AXIS2_PLACEMENT_3D('',#6842,#5619,#5620);
#4686=AXIS2_PLACEMENT_3D('',#6844,#5621,#5622);
#4687=AXIS2_PLACEMENT_3D('',#6870,#5624,#5625);
#4688=AXIS2_PLACEMENT_3D('',#6873,#5628,#5629);
#4689=AXIS2_PLACEMENT_3D('',#6875,#5631,#5632);
#4690=AXIS2_PLACEMENT_3D('',#6877,#5634,#5635);
#4691=AXIS2_PLACEMENT_3D('',#6879,#5636,#5637);
#4692=AXIS2_PLACEMENT_3D('',#6882,#5639,#5640);
#4693=AXIS2_PLACEMENT_3D('',#6883,#5641,#5642);
#4694=AXIS2_PLACEMENT_3D('',#6885,#5644,#5645);
#4695=AXIS2_PLACEMENT_3D('',#6887,#5647,#5648);
#4696=AXIS2_PLACEMENT_3D('',#6888,#5649,#5650);
#4697=AXIS2_PLACEMENT_3D('',#6889,#5651,#5652);
#5612=DIRECTION('axis',(0.,0.,1.));
#5613=DIRECTION('refdir',(1.,0.,0.));
#5614=DIRECTION('center_axis',(0.,1.,0.));
#5615=DIRECTION('ref_axis',(1.,0.,0.));
#5616=DIRECTION('',(0.866025403784439,-0.5,1.06057523872491E-16));
#5617=DIRECTION('center_axis',(0.,-1.,0.));
#5618=DIRECTION('ref_axis',(1.,0.,0.));
#5619=DIRECTION('center_axis',(0.,-1.,0.));
#5620=DIRECTION('ref_axis',(1.,0.,0.));
#5621=DIRECTION('center_axis',(0.,1.,0.));
#5622=DIRECTION('ref_axis',(1.,0.,0.));
#5623=DIRECTION('',(-0.866025403784439,-0.5,-1.06057523872491E-16));
#5624=DIRECTION('center_axis',(1.20185167898973E-16,0.,-1.));
#5625=DIRECTION('ref_axis',(-1.,0.,-1.20185167898973E-16));
#5626=DIRECTION('',(0.,1.,0.));
#5627=DIRECTION('',(0.,1.,0.));
#5628=DIRECTION('center_axis',(-0.866025403784439,0.,-0.5));
#5629=DIRECTION('ref_axis',(-0.5,0.,0.866025403784439));
#5630=DIRECTION('',(0.,1.,0.));
#5631=DIRECTION('center_axis',(-0.866025403784439,0.,0.5));
#5632=DIRECTION('ref_axis',(0.5,0.,0.866025403784439));
#5633=DIRECTION('',(0.,1.,0.));
#5634=DIRECTION('center_axis',(0.,1.,0.));
#5635=DIRECTION('ref_axis',(1.,0.,0.));
#5636=DIRECTION('center_axis',(0.,1.,0.));
#5637=DIRECTION('ref_axis',(1.,0.,0.));
#5638=DIRECTION('',(0.,-1.,0.));
#5639=DIRECTION('center_axis',(0.,1.,0.));
#5640=DIRECTION('ref_axis',(1.,0.,0.));
#5641=DIRECTION('center_axis',(-2.40370335797945E-16,0.,1.));
#5642=DIRECTION('ref_axis',(1.,0.,2.40370335797945E-16));
#5643=DIRECTION('',(0.,1.,0.));
#5644=DIRECTION('center_axis',(0.866025403784439,0.,-0.5));
#5645=DIRECTION('ref_axis',(-0.5,0.,-0.866025403784439));
#5646=DIRECTION('',(0.,1.,0.));
#5647=DIRECTION('center_axis',(0.866025403784439,0.,0.5));
#5648=DIRECTION('ref_axis',(0.5,0.,-0.866025403784439));
#5649=DIRECTION('center_axis',(0.,1.,0.));
#5650=DIRECTION('ref_axis',(1.,0.,0.));
#5651=DIRECTION('center_axis',(0.,1.,0.));
#5652=DIRECTION('ref_axis',(1.,0.,0.));
#6813=CARTESIAN_POINT('',(0.,0.,0.));
#6814=CARTESIAN_POINT('Origin',(0.,0.0525042956467857,0.));
#6815=CARTESIAN_POINT('',(-0.230940107675851,0.0472735643746089,0.4));
#6816=CARTESIAN_POINT('',(0.23094010767585,0.0472735643746089,0.4));
#6817=CARTESIAN_POINT('Ctrl Pts',(-0.230940107675851,0.0472735643746089,
0.4));
#6818=CARTESIAN_POINT('Ctrl Pts',(1.11022302462516E-16,-0.0193931022920578,
0.4));
#6819=CARTESIAN_POINT('Ctrl Pts',(0.23094010767585,0.0472735643746089,0.4));
#6820=CARTESIAN_POINT('',(-0.461880215351701,0.0472735643746089,-5.6564012731995E-17));
#6821=CARTESIAN_POINT('Ctrl Pts',(-0.461880215351701,0.0472735643746089,
-5.6564012731995E-17));
#6822=CARTESIAN_POINT('Ctrl Pts',(-0.346410161513776,-0.0193931022920579,
0.2));
#6823=CARTESIAN_POINT('Ctrl Pts',(-0.230940107675851,0.0472735643746089,
0.4));
#6824=CARTESIAN_POINT('',(-0.38,-2.08166817117217E-17,-4.65365783675994E-17));
#6825=CARTESIAN_POINT('',(-0.47094010767585,0.0525042956467857,-5.7673529545534E-17));
#6826=CARTESIAN_POINT('Origin',(0.,0.,0.));
#6827=CARTESIAN_POINT('',(-0.23094010767585,0.0472735643746089,-0.4));
#6828=CARTESIAN_POINT('Ctrl Pts',(-0.23094010767585,0.0472735643746089,
-0.4));
#6829=CARTESIAN_POINT('Ctrl Pts',(-0.346410161513775,-0.0193931022920578,
-0.2));
#6830=CARTESIAN_POINT('Ctrl Pts',(-0.461880215351701,0.0472735643746089,
-5.6564012731995E-17));
#6831=CARTESIAN_POINT('',(0.23094010767585,0.0472735643746089,-0.4));
#6832=CARTESIAN_POINT('Ctrl Pts',(0.23094010767585,0.0472735643746089,-0.4));
#6833=CARTESIAN_POINT('Ctrl Pts',(0.,-0.0193931022920578,-0.4));
#6834=CARTESIAN_POINT('Ctrl Pts',(-0.23094010767585,0.0472735643746089,
-0.4));
#6835=CARTESIAN_POINT('',(0.461880215351701,0.0472735643746089,0.));
#6836=CARTESIAN_POINT('Ctrl Pts',(0.461880215351701,0.0472735643746089,
0.));
#6837=CARTESIAN_POINT('Ctrl Pts',(0.346410161513776,-0.019393102292058,
-0.2));
#6838=CARTESIAN_POINT('Ctrl Pts',(0.23094010767585,0.0472735643746089,-0.4));
#6839=CARTESIAN_POINT('Ctrl Pts',(0.23094010767585,0.0472735643746089,0.4));
#6840=CARTESIAN_POINT('Ctrl Pts',(0.346410161513776,-0.0193931022920577,
0.2));
#6841=CARTESIAN_POINT('Ctrl Pts',(0.461880215351701,0.0472735643746089,
0.));
#6842=CARTESIAN_POINT('Origin',(0.,0.417495704353214,0.));
#6843=CARTESIAN_POINT('',(-0.38,0.47,-4.65365783675994E-17));
#6844=CARTESIAN_POINT('Origin',(0.,0.47,0.));
#6845=CARTESIAN_POINT('',(-0.461880215351701,0.422726435625391,-5.6564012731995E-17));
#6846=CARTESIAN_POINT('',(-0.47094010767585,0.417495704353214,-5.7673529545534E-17));
#6847=CARTESIAN_POINT('',(-0.230940107675851,0.422726435625391,0.4));
#6848=CARTESIAN_POINT('Ctrl Pts',(-0.230940107675851,0.422726435625391,
0.4));
#6849=CARTESIAN_POINT('Ctrl Pts',(-0.346410161513776,0.489393102292058,
0.2));
#6850=CARTESIAN_POINT('Ctrl Pts',(-0.461880215351701,0.422726435625391,
-5.6564012731995E-17));
#6851=CARTESIAN_POINT('',(0.23094010767585,0.422726435625391,0.4));
#6852=CARTESIAN_POINT('Ctrl Pts',(0.23094010767585,0.422726435625391,0.4));
#6853=CARTESIAN_POINT('Ctrl Pts',(8.32667268468867E-17,0.489393102292058,
0.4));
#6854=CARTESIAN_POINT('Ctrl Pts',(-0.230940107675851,0.422726435625391,
0.4));
#6855=CARTESIAN_POINT('',(0.461880215351701,0.422726435625391,0.));
#6856=CARTESIAN_POINT('Ctrl Pts',(0.461880215351701,0.422726435625391,0.));
#6857=CARTESIAN_POINT('Ctrl Pts',(0.346410161513776,0.489393102292058,0.2));
#6858=CARTESIAN_POINT('Ctrl Pts',(0.23094010767585,0.422726435625391,0.4));
#6859=CARTESIAN_POINT('',(0.23094010767585,0.422726435625391,-0.4));
#6860=CARTESIAN_POINT('Ctrl Pts',(0.23094010767585,0.422726435625391,-0.4));
#6861=CARTESIAN_POINT('Ctrl Pts',(0.346410161513775,0.489393102292058,-0.2));
#6862=CARTESIAN_POINT('Ctrl Pts',(0.461880215351701,0.422726435625391,0.));
#6863=CARTESIAN_POINT('',(-0.23094010767585,0.422726435625391,-0.4));
#6864=CARTESIAN_POINT('Ctrl Pts',(-0.23094010767585,0.422726435625391,-0.4));
#6865=CARTESIAN_POINT('Ctrl Pts',(-5.55111512312578E-17,0.489393102292058,
-0.4));
#6866=CARTESIAN_POINT('Ctrl Pts',(0.23094010767585,0.422726435625391,-0.4));
#6867=CARTESIAN_POINT('Ctrl Pts',(-0.461880215351701,0.422726435625391,
-5.6564012731995E-17));
#6868=CARTESIAN_POINT('Ctrl Pts',(-0.346410161513776,0.489393102292058,
-0.2));
#6869=CARTESIAN_POINT('Ctrl Pts',(-0.23094010767585,0.422726435625391,-0.4));
#6870=CARTESIAN_POINT('Origin',(0.23094010767585,0.,-0.4));
#6871=CARTESIAN_POINT('',(-0.23094010767585,0.,-0.4));
#6872=CARTESIAN_POINT('',(0.23094010767585,0.,-0.4));
#6873=CARTESIAN_POINT('Origin',(-0.23094010767585,0.,-0.4));
#6874=CARTESIAN_POINT('',(-0.461880215351701,0.,-5.6564012731995E-17));
#6875=CARTESIAN_POINT('Origin',(-0.461880215351701,0.,-5.6564012731995E-17));
#6876=CARTESIAN_POINT('',(-0.230940107675851,0.,0.4));
#6877=CARTESIAN_POINT('Origin',(0.,0.,0.));
#6878=CARTESIAN_POINT('',(-0.2117,0.47,2.59257727379495E-17));
#6879=CARTESIAN_POINT('Origin',(0.,0.47,0.));
#6880=CARTESIAN_POINT('',(-0.2117,0.,2.59257727379495E-17));
#6881=CARTESIAN_POINT('',(-0.2117,0.,2.59257727379495E-17));
#6882=CARTESIAN_POINT('Origin',(0.,0.,0.));
#6883=CARTESIAN_POINT('Origin',(-0.230940107675851,0.,0.4));
#6884=CARTESIAN_POINT('',(0.23094010767585,0.,0.4));
#6885=CARTESIAN_POINT('Origin',(0.461880215351701,0.,0.));
#6886=CARTESIAN_POINT('',(0.461880215351701,0.,0.));
#6887=CARTESIAN_POINT('Origin',(0.23094010767585,0.,0.4));
#6888=CARTESIAN_POINT('Origin',(0.,0.47,0.));
#6889=CARTESIAN_POINT('Origin',(0.,0.,0.));
#7385=UNCERTAINTY_MEASURE_WITH_UNIT(LENGTH_MEASURE(0.001),#7426,
'DISTANCE_ACCURACY_VALUE',
'Maximum model space distance between geometric entities at asserted c
onnectivities');
#7395=UNCERTAINTY_MEASURE_WITH_UNIT(LENGTH_MEASURE(0.001),#7426,
'DISTANCE_ACCURACY_VALUE',
'Maximum model space distance between geometric entities at asserted c
onnectivities');
#7415=(
GEOMETRIC_REPRESENTATION_CONTEXT(3)
GLOBAL_UNCERTAINTY_ASSIGNED_CONTEXT((#7385))
GLOBAL_UNIT_ASSIGNED_CONTEXT((#7426,#7428,#7429))
REPRESENTATION_CONTEXT('','3D')
);
#7425=(
GEOMETRIC_REPRESENTATION_CONTEXT(3)
GLOBAL_UNCERTAINTY_ASSIGNED_CONTEXT((#7395))
GLOBAL_UNIT_ASSIGNED_CONTEXT((#7426,#7428,#7429))
REPRESENTATION_CONTEXT('','3D')
);
#7426=(
LENGTH_UNIT()
NAMED_UNIT(*)
SI_UNIT(.CENTI.,.METRE.)
);
#7428=(
NAMED_UNIT(*)
PLANE_ANGLE_UNIT()
SI_UNIT($,.RADIAN.)
);
#7429=(
NAMED_UNIT(*)
SI_UNIT($,.STERADIAN.)
SOLID_ANGLE_UNIT()
);
#7449=SHAPE_DEFINITION_REPRESENTATION(#7478,#7552);
#7478=PRODUCT_DEFINITION_SHAPE('',$,#7582);
#7552=SHAPE_REPRESENTATION('',(#4682),#7415);
#7562=PRODUCT_DEFINITION_CONTEXT('part definition',#7651,'design');
#7582=PRODUCT_DEFINITION('Hex Nut - M5','Hex Nut - M5',#7611,#7562);
#7611=PRODUCT_DEFINITION_FORMATION('',$,#7672);
#7651=APPLICATION_CONTEXT(
'Core Data for Automotive Mechanical Design Process');
#7652=PRODUCT_CONTEXT('part definition',#7651,'mechanical');
#7672=PRODUCT('Hex Nut - M5','Hex Nut - M5','Hex Nut - M5',(#7652));
#7745=COLOUR_RGB('Black',0.12,0.14,0.17);
#7746=FILL_AREA_STYLE_COLOUR('',#7745);
#7747=FILL_AREA_STYLE('',(#7746));
#7748=SURFACE_STYLE_FILL_AREA(#7747);
#7749=SURFACE_SIDE_STYLE('',(#7748));
#7750=SURFACE_STYLE_USAGE(.BOTH.,#7749);
#7751=PRESENTATION_STYLE_ASSIGNMENT((#7750));
ENDSEC;
END-ISO-10303-21;
